ISO-10303-21;
HEADER;
/* Generated by software containing ST-Developer
 * from STEP Tools, Inc. (www.steptools.com) 
 */

FILE_DESCRIPTION(
/* description */ ('Bin tilter linkage'),
/* implementation_level */ '2;1');

FILE_NAME(
/* name */ 'Screw keeper fastener (2).step',
/* time_stamp */ '2026-10-28T03:26:24-07:00',
/* author */ (''),
/* organization */ (''),
/* preprocessor_version */ 'ST-DEVELOPER v20.2',
/* originating_system */ 'Autodesk Translation Framework v15.17.0.0',
/* authorisation */ '');

FILE_SCHEMA (('AUTOMOTIVE_DESIGN { 1 0 10303 214 3 1 1 }'));
ENDSEC;

DATA;
#10=MECHANICAL_DESIGN_GEOMETRIC_PRESENTATION_REPRESENTATION('',(#880),#23728);
#668=SHAPE_REPRESENTATION_RELATIONSHIP('SRR','None',#24132,#774);
#774=ADVANCED_BREP_SHAPE_REPRESENTATION('',(#994),#23632);
#880=STYLED_ITEM('',(#24772),#994);
#994=MANIFOLD_SOLID_BREP('Body1',#12410);
#1201=FACE_BOUND('',#2942,.T.);
#1571=PLANE('',#14019);
#1572=PLANE('',#14024);
#1573=PLANE('',#14027);
#2050=FACE_OUTER_BOUND('',#2941,.T.);
#2051=FACE_OUTER_BOUND('',#2943,.T.);
#2052=FACE_OUTER_BOUND('',#2944,.T.);
#2053=FACE_OUTER_BOUND('',#2945,.T.);
#2054=FACE_OUTER_BOUND('',#2946,.T.);
#2941=EDGE_LOOP('',(#9057));
#2942=EDGE_LOOP('',(#9058));
#2943=EDGE_LOOP('',(#9059,#9060,#9061,#9062));
#2944=EDGE_LOOP('',(#9063));
#2945=EDGE_LOOP('',(#9064,#9065,#9066,#9067));
#2946=EDGE_LOOP('',(#9068));
#4029=LINE('',#20504,#4704);
#4030=LINE('',#20508,#4705);
#4704=VECTOR('',#16350,0.35);
#4705=VECTOR('',#16355,0.199999999999999);
#5361=CIRCLE('',#14020,0.35);
#5362=CIRCLE('',#14021,0.199999999999999);
#5363=CIRCLE('',#14023,0.35);
#5364=CIRCLE('',#14026,0.199999999999999);
#6185=VERTEX_POINT('',#20497);
#6186=VERTEX_POINT('',#20499);
#6187=VERTEX_POINT('',#20502);
#6188=VERTEX_POINT('',#20507);
#7268=EDGE_CURVE('',#6185,#6185,#5361,.T.);
#7269=EDGE_CURVE('',#6186,#6186,#5362,.T.);
#7270=EDGE_CURVE('',#6187,#6187,#5363,.T.);
#7271=EDGE_CURVE('',#6187,#6185,#4029,.T.);
#7272=EDGE_CURVE('',#6186,#6188,#4030,.T.);
#7273=EDGE_CURVE('',#6188,#6188,#5364,.T.);
#9057=ORIENTED_EDGE('',*,*,#7268,.F.);
#9058=ORIENTED_EDGE('',*,*,#7269,.T.);
#9059=ORIENTED_EDGE('',*,*,#7270,.F.);
#9060=ORIENTED_EDGE('',*,*,#7271,.T.);
#9061=ORIENTED_EDGE('',*,*,#7268,.T.);
#9062=ORIENTED_EDGE('',*,*,#7271,.F.);
#9063=ORIENTED_EDGE('',*,*,#7270,.T.);
#9064=ORIENTED_EDGE('',*,*,#7269,.F.);
#9065=ORIENTED_EDGE('',*,*,#7272,.T.);
#9066=ORIENTED_EDGE('',*,*,#7273,.T.);
#9067=ORIENTED_EDGE('',*,*,#7272,.F.);
#9068=ORIENTED_EDGE('',*,*,#7273,.F.);
#11348=CYLINDRICAL_SURFACE('',#14022,0.35);
#11349=CYLINDRICAL_SURFACE('',#14025,0.199999999999999);
#11775=ADVANCED_FACE('',(#2050,#1201),#1571,.F.);
#11776=ADVANCED_FACE('',(#2051),#11348,.T.);
#11777=ADVANCED_FACE('',(#2052),#1572,.T.);
#11778=ADVANCED_FACE('',(#2053),#11349,.T.);
#11779=ADVANCED_FACE('',(#2054),#1573,.F.);
#12410=CLOSED_SHELL('',(#11775,#11776,#11777,#11778,#11779));
#14018=AXIS2_PLACEMENT_3D('',#20495,#16338,#16339);
#14019=AXIS2_PLACEMENT_3D('',#20496,#16340,#16341);
#14020=AXIS2_PLACEMENT_3D('',#20498,#16342,#16343);
#14021=AXIS2_PLACEMENT_3D('',#20500,#16344,#16345);
#14022=AXIS2_PLACEMENT_3D('',#20501,#16346,#16347);
#14023=AXIS2_PLACEMENT_3D('',#20503,#16348,#16349);
#14024=AXIS2_PLACEMENT_3D('',#20505,#16351,#16352);
#14025=AXIS2_PLACEMENT_3D('',#20506,#16353,#16354);
#14026=AXIS2_PLACEMENT_3D('',#20509,#16356,#16357);
#14027=AXIS2_PLACEMENT_3D('',#20510,#16358,#16359);
#16338=DIRECTION('axis',(0.,0.,1.));
#16339=DIRECTION('refdir',(1.,0.,0.));
#16340=DIRECTION('center_axis',(1.,0.,0.));
#16341=DIRECTION('ref_axis',(0.,0.,-1.));
#16342=DIRECTION('center_axis',(1.,0.,0.));
#16343=DIRECTION('ref_axis',(0.,0.,-1.));
#16344=DIRECTION('center_axis',(1.,0.,0.));
#16345=DIRECTION('ref_axis',(0.,0.,-1.));
#16346=DIRECTION('center_axis',(1.,0.,0.));
#16347=DIRECTION('ref_axis',(0.,0.,-1.));
#16348=DIRECTION('center_axis',(1.,0.,0.));
#16349=DIRECTION('ref_axis',(0.,0.,-1.));
#16350=DIRECTION('',(-1.,0.,0.));
#16351=DIRECTION('center_axis',(1.,0.,0.));
#16352=DIRECTION('ref_axis',(0.,0.,-1.));
#16353=DIRECTION('center_axis',(1.,0.,0.));
#16354=DIRECTION('ref_axis',(0.,0.,-1.));
#16355=DIRECTION('',(-1.,0.,0.));
#16356=DIRECTION('center_axis',(1.,0.,0.));
#16357=DIRECTION('ref_axis',(0.,0.,-1.));
#16358=DIRECTION('center_axis',(1.,0.,0.));
#16359=DIRECTION('ref_axis',(0.,0.,-1.));
#20495=CARTESIAN_POINT('',(0.,0.,0.));
#20496=CARTESIAN_POINT('Origin',(-8.8,-4.5,9.85));
#20497=CARTESIAN_POINT('',(-8.8,-4.5,10.2));
#20498=CARTESIAN_POINT('Origin',(-8.8,-4.5,9.85));
#20499=CARTESIAN_POINT('',(-8.8,-4.5,10.05));
#20500=CARTESIAN_POINT('Origin',(-8.8,-4.5,9.85));
#20501=CARTESIAN_POINT('Origin',(-8.8,-4.5,9.85));
#20502=CARTESIAN_POINT('',(-8.4,-4.5,10.2));
#20503=CARTESIAN_POINT('Origin',(-8.4,-4.5,9.85));
#20504=CARTESIAN_POINT('',(-8.8,-4.5,10.2));
#20505=CARTESIAN_POINT('Origin',(-8.4,-4.5,9.85));
#20506=CARTESIAN_POINT('Origin',(-9.5,-4.5,9.85));
#20507=CARTESIAN_POINT('',(-9.5,-4.5,10.05));
#20508=CARTESIAN_POINT('',(-9.5,-4.5,10.05));
#20509=CARTESIAN_POINT('Origin',(-9.5,-4.5,9.85));
#20510=CARTESIAN_POINT('Origin',(-9.5,-4.5,9.85));
#23515=UNCERTAINTY_MEASURE_WITH_UNIT(LENGTH_MEASURE(0.001),#23729,
'DISTANCE_ACCURACY_VALUE',
'Maximum model space distance between geometric entities at asserted c
onnectivities');
#23611=UNCERTAINTY_MEASURE_WITH_UNIT(LENGTH_MEASURE(0.001),#23729,
'DISTANCE_ACCURACY_VALUE',
'Maximum model space distance between geometric entities at asserted c
onnectivities');
#23632=(
GEOMETRIC_REPRESENTATION_CONTEXT(3)
GLOBAL_UNCERTAINTY_ASSIGNED_CONTEXT((#23515))
GLOBAL_UNIT_ASSIGNED_CONTEXT((#23729,#23731,#23732))
REPRESENTATION_CONTEXT('','3D')
);
#23728=(
GEOMETRIC_REPRESENTATION_CONTEXT(3)
GLOBAL_UNCERTAINTY_ASSIGNED_CONTEXT((#23611))
GLOBAL_UNIT_ASSIGNED_CONTEXT((#23729,#23731,#23732))
REPRESENTATION_CONTEXT('','3D')
);
#23729=(
LENGTH_UNIT()
NAMED_UNIT(*)
SI_UNIT(.CENTI.,.METRE.)
);
#23731=(
NAMED_UNIT(*)
PLANE_ANGLE_UNIT()
SI_UNIT($,.RADIAN.)
);
#23732=(
NAMED_UNIT(*)
SI_UNIT($,.STERADIAN.)
SOLID_ANGLE_UNIT()
);
#23753=SHAPE_DEFINITION_REPRESENTATION(#23869,#24132);
#23869=PRODUCT_DEFINITION_SHAPE('',$,#24249);
#24132=SHAPE_REPRESENTATION('',(#14018),#23632);
#24228=PRODUCT_DEFINITION_CONTEXT('part definition',#24578,'design');
#24249=PRODUCT_DEFINITION('Screw keeper fastener (2)',
'Screw keeper fastener (2)',#24365,#24228);
#24365=PRODUCT_DEFINITION_FORMATION('',$,#24600);
#24578=APPLICATION_CONTEXT(
'Core Data for Automotive Mechanical Design Process');
#24579=PRODUCT_CONTEXT('part definition',#24578,'mechanical');
#24600=PRODUCT('Screw keeper fastener (2)','Screw keeper fastener (2)',
'Screw keeper fastener (2)',(#24579));
#24766=COLOUR_RGB('Black',0.12,0.14,0.17);
#24767=FILL_AREA_STYLE_COLOUR('',#24766);
#24768=FILL_AREA_STYLE('',(#24767));
#24769=SURFACE_STYLE_FILL_AREA(#24768);
#24770=SURFACE_SIDE_STYLE('',(#24769));
#24771=SURFACE_STYLE_USAGE(.BOTH.,#24770);
#24772=PRESENTATION_STYLE_ASSIGNMENT((#24771));
ENDSEC;
END-ISO-10303-21;
